ISO-10303-21;
HEADER;
/* Generated by software containing ST-Developer
 * from STEP Tools, Inc. (www.steptools.com) 
 */

FILE_DESCRIPTION(
/* description */ ('Four-bar parallelogram arm'),
/* implementation_level */ '2;1');

FILE_NAME(
/* name */ 'Rear inner spacer (3).step',
/* time_stamp */ '2026-10-28T03:24:55-07:00',
/* author */ (''),
/* organization */ (''),
/* preprocessor_version */ 'ST-DEVELOPER v20.2',
/* originating_system */ 'Autodesk Translation Framework v15.17.0.0',
/* authorisation */ '');

FILE_SCHEMA (('AUTOMOTIVE_DESIGN { 1 0 10303 214 3 1 1 }'));
ENDSEC;

DATA;
#10=MECHANICAL_DESIGN_GEOMETRIC_PRESENTATION_REPRESENTATION('',(#676),#14512);
#568=SHAPE_REPRESENTATION_RELATIONSHIP('SRR','None',#14793,#618);
#618=ADVANCED_BREP_SHAPE_REPRESENTATION('',(#732),#14508);
#676=STYLED_ITEM('',(#15080),#732);
#732=MANIFOLD_SOLID_BREP('Body1',#7382);
#999=FACE_BOUND('',#2279,.T.);
#1000=FACE_BOUND('',#2281,.T.);
#1184=PLANE('',#8872);
#1185=PLANE('',#8873);
#1592=FACE_OUTER_BOUND('',#2276,.T.);
#1593=FACE_OUTER_BOUND('',#2277,.T.);
#1594=FACE_OUTER_BOUND('',#2278,.T.);
#1595=FACE_OUTER_BOUND('',#2280,.T.);
#2276=EDGE_LOOP('',(#6614,#6615,#6616,#6617));
#2277=EDGE_LOOP('',(#6618,#6619,#6620,#6621));
#2278=EDGE_LOOP('',(#6622));
#2279=EDGE_LOOP('',(#6623));
#2280=EDGE_LOOP('',(#6624));
#2281=EDGE_LOOP('',(#6625));
#2676=LINE('',#14237,#3070);
#2677=LINE('',#14243,#3071);
#3070=VECTOR('',#11194,0.504999999999999);
#3071=VECTOR('',#11201,0.699999999999999);
#3525=CIRCLE('',#8867,0.504999999999999);
#3526=CIRCLE('',#8868,0.504999999999999);
#3527=CIRCLE('',#8870,0.699999999999999);
#3528=CIRCLE('',#8871,0.699999999999999);
#4093=VERTEX_POINT('',#14234);
#4094=VERTEX_POINT('',#14236);
#4095=VERTEX_POINT('',#14240);
#4096=VERTEX_POINT('',#14242);
#4938=EDGE_CURVE('',#4093,#4093,#3525,.T.);
#4939=EDGE_CURVE('',#4093,#4094,#2676,.T.);
#4940=EDGE_CURVE('',#4094,#4094,#3526,.T.);
#4941=EDGE_CURVE('',#4095,#4095,#3527,.T.);
#4942=EDGE_CURVE('',#4095,#4096,#2677,.T.);
#4943=EDGE_CURVE('',#4096,#4096,#3528,.T.);
#6614=ORIENTED_EDGE('',*,*,#4938,.F.);
#6615=ORIENTED_EDGE('',*,*,#4939,.T.);
#6616=ORIENTED_EDGE('',*,*,#4940,.T.);
#6617=ORIENTED_EDGE('',*,*,#4939,.F.);
#6618=ORIENTED_EDGE('',*,*,#4941,.F.);
#6619=ORIENTED_EDGE('',*,*,#4942,.T.);
#6620=ORIENTED_EDGE('',*,*,#4943,.T.);
#6621=ORIENTED_EDGE('',*,*,#4942,.F.);
#6622=ORIENTED_EDGE('',*,*,#4941,.T.);
#6623=ORIENTED_EDGE('',*,*,#4938,.T.);
#6624=ORIENTED_EDGE('',*,*,#4943,.F.);
#6625=ORIENTED_EDGE('',*,*,#4940,.F.);
#6898=CYLINDRICAL_SURFACE('',#8866,0.504999999999999);
#6899=CYLINDRICAL_SURFACE('',#8869,0.699999999999999);
#7297=ADVANCED_FACE('',(#1592),#6898,.F.);
#7298=ADVANCED_FACE('',(#1593),#6899,.T.);
#7299=ADVANCED_FACE('',(#1594,#999),#1184,.T.);
#7300=ADVANCED_FACE('',(#1595,#1000),#1185,.F.);
#7382=CLOSED_SHELL('',(#7297,#7298,#7299,#7300));
#8865=AXIS2_PLACEMENT_3D('',#14232,#11188,#11189);
#8866=AXIS2_PLACEMENT_3D('',#14233,#11190,#11191);
#8867=AXIS2_PLACEMENT_3D('',#14235,#11192,#11193);
#8868=AXIS2_PLACEMENT_3D('',#14238,#11195,#11196);
#8869=AXIS2_PLACEMENT_3D('',#14239,#11197,#11198);
#8870=AXIS2_PLACEMENT_3D('',#14241,#11199,#11200);
#8871=AXIS2_PLACEMENT_3D('',#14244,#11202,#11203);
#8872=AXIS2_PLACEMENT_3D('',#14245,#11204,#11205);
#8873=AXIS2_PLACEMENT_3D('',#14246,#11206,#11207);
#11188=DIRECTION('axis',(0.,0.,1.));
#11189=DIRECTION('refdir',(1.,0.,0.));
#11190=DIRECTION('center_axis',(0.,1.,0.));
#11191=DIRECTION('ref_axis',(1.,0.,0.));
#11192=DIRECTION('center_axis',(0.,-1.,0.));
#11193=DIRECTION('ref_axis',(1.,0.,0.));
#11194=DIRECTION('',(0.,-1.,0.));
#11195=DIRECTION('center_axis',(0.,-1.,0.));
#11196=DIRECTION('ref_axis',(1.,0.,0.));
#11197=DIRECTION('center_axis',(0.,1.,0.));
#11198=DIRECTION('ref_axis',(1.,0.,0.));
#11199=DIRECTION('center_axis',(0.,1.,0.));
#11200=DIRECTION('ref_axis',(1.,0.,0.));
#11201=DIRECTION('',(0.,-1.,0.));
#11202=DIRECTION('center_axis',(0.,1.,0.));
#11203=DIRECTION('ref_axis',(1.,0.,0.));
#11204=DIRECTION('center_axis',(0.,1.,0.));
#11205=DIRECTION('ref_axis',(1.,0.,0.));
#11206=DIRECTION('center_axis',(0.,1.,0.));
#11207=DIRECTION('ref_axis',(1.,0.,0.));
#14232=CARTESIAN_POINT('',(0.,0.,0.));
#14233=CARTESIAN_POINT('Origin',(20.,1.05,14.));
#14234=CARTESIAN_POINT('',(19.495,2.5,14.));
#14235=CARTESIAN_POINT('Origin',(20.,2.5,14.));
#14236=CARTESIAN_POINT('',(19.495,1.05,14.));
#14237=CARTESIAN_POINT('',(19.495,1.05,14.));
#14238=CARTESIAN_POINT('Origin',(20.,1.05,14.));
#14239=CARTESIAN_POINT('Origin',(20.,1.05,14.));
#14240=CARTESIAN_POINT('',(19.3,2.5,14.));
#14241=CARTESIAN_POINT('Origin',(20.,2.5,14.));
#14242=CARTESIAN_POINT('',(19.3,1.05,14.));
#14243=CARTESIAN_POINT('',(19.3,1.05,14.));
#14244=CARTESIAN_POINT('Origin',(20.,1.05,14.));
#14245=CARTESIAN_POINT('Origin',(20.,2.5,14.));
#14246=CARTESIAN_POINT('Origin',(20.,1.05,14.));
#14451=UNCERTAINTY_MEASURE_WITH_UNIT(LENGTH_MEASURE(0.001),#14513,
'DISTANCE_ACCURACY_VALUE',
'Maximum model space distance between geometric entities at asserted c
onnectivities');
#14455=UNCERTAINTY_MEASURE_WITH_UNIT(LENGTH_MEASURE(0.001),#14513,
'DISTANCE_ACCURACY_VALUE',
'Maximum model space distance between geometric entities at asserted c
onnectivities');
#14508=(
GEOMETRIC_REPRESENTATION_CONTEXT(3)
GLOBAL_UNCERTAINTY_ASSIGNED_CONTEXT((#14451))
GLOBAL_UNIT_ASSIGNED_CONTEXT((#14513,#14515,#14516))
REPRESENTATION_CONTEXT('','3D')
);
#14512=(
GEOMETRIC_REPRESENTATION_CONTEXT(3)
GLOBAL_UNCERTAINTY_ASSIGNED_CONTEXT((#14455))
GLOBAL_UNIT_ASSIGNED_CONTEXT((#14513,#14515,#14516))
REPRESENTATION_CONTEXT('','3D')
);
#14513=(
LENGTH_UNIT()
NAMED_UNIT(*)
SI_UNIT(.CENTI.,.METRE.)
);
#14515=(
NAMED_UNIT(*)
PLANE_ANGLE_UNIT()
SI_UNIT($,.RADIAN.)
);
#14516=(
NAMED_UNIT(*)
SI_UNIT($,.STERADIAN.)
SOLID_ANGLE_UNIT()
);
#14569=SHAPE_DEFINITION_REPRESENTATION(#14685,#14793);
#14685=PRODUCT_DEFINITION_SHAPE('',$,#14850);
#14793=SHAPE_REPRESENTATION('',(#8865),#14508);
#14797=PRODUCT_DEFINITION_CONTEXT('part definition',#14967,'design');
#14850=PRODUCT_DEFINITION('Rear inner spacer (3)','Rear inner spacer (3)',
#14906,#14797);
#14906=PRODUCT_DEFINITION_FORMATION('',$,#15021);
#14967=APPLICATION_CONTEXT(
'Core Data for Automotive Mechanical Design Process');
#14968=PRODUCT_CONTEXT('part definition',#14967,'mechanical');
#15021=PRODUCT('Rear inner spacer (3)','Rear inner spacer (3)',
'Rear inner spacer (3)',(#14968));
#15074=COLOUR_RGB('Sky Blue',0.24,0.69,0.87);
#15075=FILL_AREA_STYLE_COLOUR('',#15074);
#15076=FILL_AREA_STYLE('',(#15075));
#15077=SURFACE_STYLE_FILL_AREA(#15076);
#15078=SURFACE_SIDE_STYLE('',(#15077));
#15079=SURFACE_STYLE_USAGE(.BOTH.,#15078);
#15080=PRESENTATION_STYLE_ASSIGNMENT((#15079));
ENDSEC;
END-ISO-10303-21;
